ISO-10303-21;
HEADER;
/* Generated by software containing ST-Developer
 * from STEP Tools, Inc. (www.steptools.com) 
 */

FILE_DESCRIPTION(
/* description */ ('Gravity roller conveyor section'),
/* implementation_level */ '2;1');

FILE_NAME(
/* name */ 'Bearing insert (1).step',
/* time_stamp */ '2026-11-02T07:43:02-08:00',
/* author */ (''),
/* organization */ (''),
/* preprocessor_version */ 'ST-DEVELOPER v20.2',
/* originating_system */ 'Autodesk Translation Framework v15.17.0.0',
/* authorisation */ '');

FILE_SCHEMA (('AUTOMOTIVE_DESIGN { 1 0 10303 214 3 1 1 }'));
ENDSEC;

DATA;
#10=MECHANICAL_DESIGN_GEOMETRIC_PRESENTATION_REPRESENTATION('',(#546),#13821);
#478=SHAPE_REPRESENTATION_RELATIONSHIP('SRR','None',#14016,#512);
#512=ADVANCED_BREP_SHAPE_REPRESENTATION('',(#586),#13803);
#546=STYLED_ITEM('',(#14191),#586);
#586=MANIFOLD_SOLID_BREP('Body1',#7646);
#658=FACE_BOUND('',#1738,.T.);
#659=FACE_BOUND('',#1742,.T.);
#660=FACE_BOUND('',#1744,.T.);
#921=PLANE('',#8405);
#922=PLANE('',#8412);
#923=PLANE('',#8413);
#1268=FACE_OUTER_BOUND('',#1736,.T.);
#1269=FACE_OUTER_BOUND('',#1737,.T.);
#1270=FACE_OUTER_BOUND('',#1739,.T.);
#1271=FACE_OUTER_BOUND('',#1740,.T.);
#1272=FACE_OUTER_BOUND('',#1741,.T.);
#1273=FACE_OUTER_BOUND('',#1743,.T.);
#1736=EDGE_LOOP('',(#6510,#6511,#6512,#6513));
#1737=EDGE_LOOP('',(#6514));
#1738=EDGE_LOOP('',(#6515));
#1739=EDGE_LOOP('',(#6516,#6517,#6518,#6519));
#1740=EDGE_LOOP('',(#6520,#6521,#6522,#6523));
#1741=EDGE_LOOP('',(#6524));
#1742=EDGE_LOOP('',(#6525));
#1743=EDGE_LOOP('',(#6526));
#1744=EDGE_LOOP('',(#6527));
#2510=LINE('',#12617,#3228);
#2511=LINE('',#12625,#3229);
#2512=LINE('',#12630,#3230);
#3228=VECTOR('',#10101,1.1);
#3229=VECTOR('',#10112,1.5);
#3230=VECTOR('',#10117,1.7);
#3446=CIRCLE('',#8403,1.1);
#3447=CIRCLE('',#8404,1.1);
#3448=CIRCLE('',#8406,1.5);
#3449=CIRCLE('',#8408,1.5);
#3450=CIRCLE('',#8410,1.7);
#3451=CIRCLE('',#8411,1.7);
#4024=VERTEX_POINT('',#12614);
#4025=VERTEX_POINT('',#12616);
#4026=VERTEX_POINT('',#12620);
#4027=VERTEX_POINT('',#12623);
#4028=VERTEX_POINT('',#12627);
#4029=VERTEX_POINT('',#12629);
#4892=EDGE_CURVE('',#4024,#4024,#3446,.T.);
#4893=EDGE_CURVE('',#4024,#4025,#2510,.T.);
#4894=EDGE_CURVE('',#4025,#4025,#3447,.T.);
#4895=EDGE_CURVE('',#4026,#4026,#3448,.T.);
#4896=EDGE_CURVE('',#4027,#4027,#3449,.T.);
#4897=EDGE_CURVE('',#4027,#4026,#2511,.T.);
#4898=EDGE_CURVE('',#4028,#4028,#3450,.T.);
#4899=EDGE_CURVE('',#4028,#4029,#2512,.T.);
#4900=EDGE_CURVE('',#4029,#4029,#3451,.T.);
#6510=ORIENTED_EDGE('',*,*,#4892,.F.);
#6511=ORIENTED_EDGE('',*,*,#4893,.T.);
#6512=ORIENTED_EDGE('',*,*,#4894,.T.);
#6513=ORIENTED_EDGE('',*,*,#4893,.F.);
#6514=ORIENTED_EDGE('',*,*,#4895,.F.);
#6515=ORIENTED_EDGE('',*,*,#4892,.T.);
#6516=ORIENTED_EDGE('',*,*,#4896,.F.);
#6517=ORIENTED_EDGE('',*,*,#4897,.T.);
#6518=ORIENTED_EDGE('',*,*,#4895,.T.);
#6519=ORIENTED_EDGE('',*,*,#4897,.F.);
#6520=ORIENTED_EDGE('',*,*,#4898,.F.);
#6521=ORIENTED_EDGE('',*,*,#4899,.T.);
#6522=ORIENTED_EDGE('',*,*,#4900,.T.);
#6523=ORIENTED_EDGE('',*,*,#4899,.F.);
#6524=ORIENTED_EDGE('',*,*,#4898,.T.);
#6525=ORIENTED_EDGE('',*,*,#4896,.T.);
#6526=ORIENTED_EDGE('',*,*,#4900,.F.);
#6527=ORIENTED_EDGE('',*,*,#4894,.F.);
#7164=CYLINDRICAL_SURFACE('',#8402,1.1);
#7165=CYLINDRICAL_SURFACE('',#8407,1.5);
#7166=CYLINDRICAL_SURFACE('',#8409,1.7);
#7469=ADVANCED_FACE('',(#1268),#7164,.F.);
#7470=ADVANCED_FACE('',(#1269,#658),#921,.T.);
#7471=ADVANCED_FACE('',(#1270),#7165,.F.);
#7472=ADVANCED_FACE('',(#1271),#7166,.T.);
#7473=ADVANCED_FACE('',(#1272,#659),#922,.T.);
#7474=ADVANCED_FACE('',(#1273,#660),#923,.F.);
#7646=CLOSED_SHELL('',(#7469,#7470,#7471,#7472,#7473,#7474));
#8401=AXIS2_PLACEMENT_3D('',#12612,#10095,#10096);
#8402=AXIS2_PLACEMENT_3D('',#12613,#10097,#10098);
#8403=AXIS2_PLACEMENT_3D('',#12615,#10099,#10100);
#8404=AXIS2_PLACEMENT_3D('',#12618,#10102,#10103);
#8405=AXIS2_PLACEMENT_3D('',#12619,#10104,#10105);
#8406=AXIS2_PLACEMENT_3D('',#12621,#10106,#10107);
#8407=AXIS2_PLACEMENT_3D('',#12622,#10108,#10109);
#8408=AXIS2_PLACEMENT_3D('',#12624,#10110,#10111);
#8409=AXIS2_PLACEMENT_3D('',#12626,#10113,#10114);
#8410=AXIS2_PLACEMENT_3D('',#12628,#10115,#10116);
#8411=AXIS2_PLACEMENT_3D('',#12631,#10118,#10119);
#8412=AXIS2_PLACEMENT_3D('',#12632,#10120,#10121);
#8413=AXIS2_PLACEMENT_3D('',#12633,#10122,#10123);
#10095=DIRECTION('axis',(0.,0.,1.));
#10096=DIRECTION('refdir',(1.,0.,0.));
#10097=DIRECTION('center_axis',(0.,1.,0.));
#10098=DIRECTION('ref_axis',(1.,0.,0.));
#10099=DIRECTION('center_axis',(0.,-1.,0.));
#10100=DIRECTION('ref_axis',(1.,0.,0.));
#10101=DIRECTION('',(0.,-1.,0.));
#10102=DIRECTION('center_axis',(0.,-1.,0.));
#10103=DIRECTION('ref_axis',(1.,0.,0.));
#10104=DIRECTION('center_axis',(0.,1.,0.));
#10105=DIRECTION('ref_axis',(1.,0.,0.));
#10106=DIRECTION('center_axis',(0.,-1.,0.));
#10107=DIRECTION('ref_axis',(1.,0.,0.));
#10108=DIRECTION('center_axis',(0.,1.,0.));
#10109=DIRECTION('ref_axis',(1.,0.,0.));
#10110=DIRECTION('center_axis',(0.,-1.,0.));
#10111=DIRECTION('ref_axis',(1.,0.,0.));
#10112=DIRECTION('',(0.,-1.,0.));
#10113=DIRECTION('center_axis',(0.,1.,0.));
#10114=DIRECTION('ref_axis',(1.,0.,0.));
#10115=DIRECTION('center_axis',(0.,1.,0.));
#10116=DIRECTION('ref_axis',(1.,0.,0.));
#10117=DIRECTION('',(0.,-1.,0.));
#10118=DIRECTION('center_axis',(0.,1.,0.));
#10119=DIRECTION('ref_axis',(1.,0.,0.));
#10120=DIRECTION('center_axis',(0.,1.,0.));
#10121=DIRECTION('ref_axis',(1.,0.,0.));
#10122=DIRECTION('center_axis',(0.,1.,0.));
#10123=DIRECTION('ref_axis',(1.,0.,0.));
#12612=CARTESIAN_POINT('',(0.,0.,0.));
#12613=CARTESIAN_POINT('Origin',(3.,28.8,8.));
#12614=CARTESIAN_POINT('',(1.9,29.05,8.));
#12615=CARTESIAN_POINT('Origin',(3.,29.05,8.));
#12616=CARTESIAN_POINT('',(1.9,28.8,8.));
#12617=CARTESIAN_POINT('',(1.9,28.8,8.));
#12618=CARTESIAN_POINT('Origin',(3.,28.8,8.));
#12619=CARTESIAN_POINT('Origin',(3.,29.05,8.));
#12620=CARTESIAN_POINT('',(1.5,29.05,8.));
#12621=CARTESIAN_POINT('Origin',(3.,29.05,8.));
#12622=CARTESIAN_POINT('Origin',(3.,28.8,8.));
#12623=CARTESIAN_POINT('',(1.5,30.,8.));
#12624=CARTESIAN_POINT('Origin',(3.,30.,8.));
#12625=CARTESIAN_POINT('',(1.5,28.8,8.));
#12626=CARTESIAN_POINT('Origin',(3.,28.8,8.));
#12627=CARTESIAN_POINT('',(1.3,30.,8.));
#12628=CARTESIAN_POINT('Origin',(3.,30.,8.));
#12629=CARTESIAN_POINT('',(1.3,28.8,8.));
#12630=CARTESIAN_POINT('',(1.3,28.8,8.));
#12631=CARTESIAN_POINT('Origin',(3.,28.8,8.));
#12632=CARTESIAN_POINT('Origin',(3.,30.,8.));
#12633=CARTESIAN_POINT('Origin',(3.,28.8,8.));
#13764=UNCERTAINTY_MEASURE_WITH_UNIT(LENGTH_MEASURE(0.001),#13822,
'DISTANCE_ACCURACY_VALUE',
'Maximum model space distance between geometric entities at asserted c
onnectivities');
#13782=UNCERTAINTY_MEASURE_WITH_UNIT(LENGTH_MEASURE(0.001),#13822,
'DISTANCE_ACCURACY_VALUE',
'Maximum model space distance between geometric entities at asserted c
onnectivities');
#13803=(
GEOMETRIC_REPRESENTATION_CONTEXT(3)
GLOBAL_UNCERTAINTY_ASSIGNED_CONTEXT((#13764))
GLOBAL_UNIT_ASSIGNED_CONTEXT((#13822,#13824,#13825))
REPRESENTATION_CONTEXT('','3D')
);
#13821=(
GEOMETRIC_REPRESENTATION_CONTEXT(3)
GLOBAL_UNCERTAINTY_ASSIGNED_CONTEXT((#13782))
GLOBAL_UNIT_ASSIGNED_CONTEXT((#13822,#13824,#13825))
REPRESENTATION_CONTEXT('','3D')
);
#13822=(
LENGTH_UNIT()
NAMED_UNIT(*)
SI_UNIT(.CENTI.,.METRE.)
);
#13824=(
NAMED_UNIT(*)
PLANE_ANGLE_UNIT()
SI_UNIT($,.RADIAN.)
);
#13825=(
NAMED_UNIT(*)
SI_UNIT($,.STERADIAN.)
SOLID_ANGLE_UNIT()
);
#13846=SHAPE_DEFINITION_REPRESENTATION(#13884,#14016);
#13884=PRODUCT_DEFINITION_SHAPE('',$,#14055);
#14016=SHAPE_REPRESENTATION('',(#8401),#13803);
#14034=PRODUCT_DEFINITION_CONTEXT('part definition',#14150,'design');
#14055=PRODUCT_DEFINITION('Bearing insert_1','Bearing insert (1)',#14093,
#14034);
#14093=PRODUCT_DEFINITION_FORMATION('',$,#14172);
#14150=APPLICATION_CONTEXT(
'Core Data for Automotive Mechanical Design Process');
#14151=PRODUCT_CONTEXT('part definition',#14150,'mechanical');
#14172=PRODUCT('Bearing insert_1','Bearing insert (1)','Bearing insert',
(#14151));
#14191=PRESENTATION_STYLE_ASSIGNMENT((#14196));
#14196=SURFACE_STYLE_USAGE(.BOTH.,#14201);
#14201=SURFACE_SIDE_STYLE('',(#14206));
#14206=SURFACE_STYLE_FILL_AREA(#14211);
#14211=FILL_AREA_STYLE('CAD Library Painted - Steel gray',(#14216));
#14216=FILL_AREA_STYLE_COLOUR('CAD Library Painted - Steel gray',#14221);
#14221=COLOUR_RGB('CAD Library Painted - Steel gray',0.592156862745098,
0.631372549019608,0.67843137254902);
ENDSEC;
END-ISO-10303-21;
